ISO-10303-21;
HEADER;
/* Generated by software containing ST-Developer
 * from STEP Tools, Inc. (www.steptools.com) 
 */

FILE_DESCRIPTION(
/* description */ ('Crank-driven oscillating fan base (mechanism only)'),

/* implementation_level */ '2;1');

FILE_NAME(
/* name */ 'Foot strip (1).step',
/* time_stamp */ '2026-10-28T03:25:00-07:00',
/* author */ (''),
/* organization */ (''),
/* preprocessor_version */ 'ST-DEVELOPER v20.2',
/* originating_system */ 'Autodesk Translation Framework v15.17.0.0',
/* authorisation */ '');

FILE_SCHEMA (('AUTOMOTIVE_DESIGN { 1 0 10303 214 3 1 1 }'));
ENDSEC;

DATA;
#10=MECHANICAL_DESIGN_GEOMETRIC_PRESENTATION_REPRESENTATION('',(#439),#11916);
#359=SHAPE_REPRESENTATION_RELATIONSHIP('SRR','None',#12083,#399);
#399=ADVANCED_BREP_SHAPE_REPRESENTATION('',(#487),#11874);
#439=STYLED_ITEM('',(#12361),#487);
#487=MANIFOLD_SOLID_BREP('Body1',#6069);
#704=PLANE('',#6600);
#705=PLANE('',#6601);
#706=PLANE('',#6602);
#707=PLANE('',#6603);
#708=PLANE('',#6604);
#709=PLANE('',#6605);
#906=FACE_OUTER_BOUND('',#1297,.T.);
#907=FACE_OUTER_BOUND('',#1298,.T.);
#908=FACE_OUTER_BOUND('',#1299,.T.);
#909=FACE_OUTER_BOUND('',#1300,.T.);
#910=FACE_OUTER_BOUND('',#1301,.T.);
#911=FACE_OUTER_BOUND('',#1302,.T.);
#1297=EDGE_LOOP('',(#4164,#4165,#4166,#4167));
#1298=EDGE_LOOP('',(#4168,#4169,#4170,#4171));
#1299=EDGE_LOOP('',(#4172,#4173,#4174,#4175));
#1300=EDGE_LOOP('',(#4176,#4177,#4178,#4179));
#1301=EDGE_LOOP('',(#4180,#4181,#4182,#4183));
#1302=EDGE_LOOP('',(#4184,#4185,#4186,#4187));
#1830=LINE('',#9556,#2163);
#1831=LINE('',#9558,#2164);
#1832=LINE('',#9560,#2165);
#1833=LINE('',#9561,#2166);
#1834=LINE('',#9564,#2167);
#1835=LINE('',#9566,#2168);
#1836=LINE('',#9567,#2169);
#1837=LINE('',#9570,#2170);
#1838=LINE('',#9572,#2171);
#1839=LINE('',#9573,#2172);
#1840=LINE('',#9575,#2173);
#1841=LINE('',#9576,#2174);
#2163=VECTOR('',#7527,1.);
#2164=VECTOR('',#7528,1.);
#2165=VECTOR('',#7529,1.);
#2166=VECTOR('',#7530,1.);
#2167=VECTOR('',#7533,1.);
#2168=VECTOR('',#7534,1.);
#2169=VECTOR('',#7535,1.);
#2170=VECTOR('',#7538,1.);
#2171=VECTOR('',#7539,1.);
#2172=VECTOR('',#7540,1.);
#2173=VECTOR('',#7543,1.);
#2174=VECTOR('',#7544,1.);
#2861=VERTEX_POINT('',#9554);
#2862=VERTEX_POINT('',#9555);
#2863=VERTEX_POINT('',#9557);
#2864=VERTEX_POINT('',#9559);
#2865=VERTEX_POINT('',#9563);
#2866=VERTEX_POINT('',#9565);
#2867=VERTEX_POINT('',#9569);
#2868=VERTEX_POINT('',#9571);
#3377=EDGE_CURVE('',#2861,#2862,#1830,.T.);
#3378=EDGE_CURVE('',#2862,#2863,#1831,.T.);
#3379=EDGE_CURVE('',#2864,#2863,#1832,.T.);
#3380=EDGE_CURVE('',#2861,#2864,#1833,.T.);
#3381=EDGE_CURVE('',#2865,#2861,#1834,.T.);
#3382=EDGE_CURVE('',#2866,#2864,#1835,.T.);
#3383=EDGE_CURVE('',#2865,#2866,#1836,.T.);
#3384=EDGE_CURVE('',#2867,#2865,#1837,.T.);
#3385=EDGE_CURVE('',#2868,#2866,#1838,.T.);
#3386=EDGE_CURVE('',#2867,#2868,#1839,.T.);
#3387=EDGE_CURVE('',#2862,#2867,#1840,.T.);
#3388=EDGE_CURVE('',#2863,#2868,#1841,.T.);
#4164=ORIENTED_EDGE('',*,*,#3377,.T.);
#4165=ORIENTED_EDGE('',*,*,#3378,.T.);
#4166=ORIENTED_EDGE('',*,*,#3379,.F.);
#4167=ORIENTED_EDGE('',*,*,#3380,.F.);
#4168=ORIENTED_EDGE('',*,*,#3381,.T.);
#4169=ORIENTED_EDGE('',*,*,#3380,.T.);
#4170=ORIENTED_EDGE('',*,*,#3382,.F.);
#4171=ORIENTED_EDGE('',*,*,#3383,.F.);
#4172=ORIENTED_EDGE('',*,*,#3384,.T.);
#4173=ORIENTED_EDGE('',*,*,#3383,.T.);
#4174=ORIENTED_EDGE('',*,*,#3385,.F.);
#4175=ORIENTED_EDGE('',*,*,#3386,.F.);
#4176=ORIENTED_EDGE('',*,*,#3387,.T.);
#4177=ORIENTED_EDGE('',*,*,#3386,.T.);
#4178=ORIENTED_EDGE('',*,*,#3388,.F.);
#4179=ORIENTED_EDGE('',*,*,#3378,.F.);
#4180=ORIENTED_EDGE('',*,*,#3388,.T.);
#4181=ORIENTED_EDGE('',*,*,#3385,.T.);
#4182=ORIENTED_EDGE('',*,*,#3382,.T.);
#4183=ORIENTED_EDGE('',*,*,#3379,.T.);
#4184=ORIENTED_EDGE('',*,*,#3387,.F.);
#4185=ORIENTED_EDGE('',*,*,#3377,.F.);
#4186=ORIENTED_EDGE('',*,*,#3381,.F.);
#4187=ORIENTED_EDGE('',*,*,#3384,.F.);
#5712=ADVANCED_FACE('',(#906),#704,.T.);
#5713=ADVANCED_FACE('',(#907),#705,.T.);
#5714=ADVANCED_FACE('',(#908),#706,.T.);
#5715=ADVANCED_FACE('',(#909),#707,.T.);
#5716=ADVANCED_FACE('',(#910),#708,.T.);
#5717=ADVANCED_FACE('',(#911),#709,.F.);
#6069=CLOSED_SHELL('',(#5712,#5713,#5714,#5715,#5716,#5717));
#6599=AXIS2_PLACEMENT_3D('',#9552,#7523,#7524);
#6600=AXIS2_PLACEMENT_3D('',#9553,#7525,#7526);
#6601=AXIS2_PLACEMENT_3D('',#9562,#7531,#7532);
#6602=AXIS2_PLACEMENT_3D('',#9568,#7536,#7537);
#6603=AXIS2_PLACEMENT_3D('',#9574,#7541,#7542);
#6604=AXIS2_PLACEMENT_3D('',#9577,#7545,#7546);
#6605=AXIS2_PLACEMENT_3D('',#9578,#7547,#7548);
#7523=DIRECTION('axis',(0.,0.,1.));
#7524=DIRECTION('refdir',(1.,0.,0.));
#7525=DIRECTION('center_axis',(0.,1.,0.));
#7526=DIRECTION('ref_axis',(-1.,0.,0.));
#7527=DIRECTION('',(-1.,0.,0.));
#7528=DIRECTION('',(0.,0.,1.));
#7529=DIRECTION('',(-1.,0.,0.));
#7530=DIRECTION('',(0.,0.,1.));
#7531=DIRECTION('center_axis',(1.,0.,0.));
#7532=DIRECTION('ref_axis',(0.,1.,0.));
#7533=DIRECTION('',(0.,1.,0.));
#7534=DIRECTION('',(0.,1.,0.));
#7535=DIRECTION('',(0.,0.,1.));
#7536=DIRECTION('center_axis',(0.,-1.,0.));
#7537=DIRECTION('ref_axis',(1.,0.,0.));
#7538=DIRECTION('',(1.,0.,0.));
#7539=DIRECTION('',(1.,0.,0.));
#7540=DIRECTION('',(0.,0.,1.));
#7541=DIRECTION('center_axis',(-1.,0.,0.));
#7542=DIRECTION('ref_axis',(0.,-1.,0.));
#7543=DIRECTION('',(0.,-1.,0.));
#7544=DIRECTION('',(0.,-1.,0.));
#7545=DIRECTION('center_axis',(0.,0.,1.));
#7546=DIRECTION('ref_axis',(1.,0.,0.));
#7547=DIRECTION('center_axis',(0.,0.,1.));
#7548=DIRECTION('ref_axis',(1.,0.,0.));
#9552=CARTESIAN_POINT('',(0.,0.,0.));
#9553=CARTESIAN_POINT('Origin',(12.,6.5,-0.5));
#9554=CARTESIAN_POINT('',(12.,6.5,-0.5));
#9555=CARTESIAN_POINT('',(-4.,6.5,-0.5));
#9556=CARTESIAN_POINT('',(12.,6.5,-0.5));
#9557=CARTESIAN_POINT('',(-4.,6.5,0.));
#9558=CARTESIAN_POINT('',(-4.,6.5,-0.5));
#9559=CARTESIAN_POINT('',(12.,6.5,0.));
#9560=CARTESIAN_POINT('',(12.,6.5,0.));
#9561=CARTESIAN_POINT('',(12.,6.5,-0.5));
#9562=CARTESIAN_POINT('Origin',(12.,5.5,-0.5));
#9563=CARTESIAN_POINT('',(12.,5.5,-0.5));
#9564=CARTESIAN_POINT('',(12.,5.5,-0.5));
#9565=CARTESIAN_POINT('',(12.,5.5,0.));
#9566=CARTESIAN_POINT('',(12.,5.5,0.));
#9567=CARTESIAN_POINT('',(12.,5.5,-0.5));
#9568=CARTESIAN_POINT('Origin',(-4.,5.5,-0.5));
#9569=CARTESIAN_POINT('',(-4.,5.5,-0.5));
#9570=CARTESIAN_POINT('',(-4.,5.5,-0.5));
#9571=CARTESIAN_POINT('',(-4.,5.5,0.));
#9572=CARTESIAN_POINT('',(-4.,5.5,0.));
#9573=CARTESIAN_POINT('',(-4.,5.5,-0.5));
#9574=CARTESIAN_POINT('Origin',(-4.,6.5,-0.5));
#9575=CARTESIAN_POINT('',(-4.,6.5,-0.5));
#9576=CARTESIAN_POINT('',(-4.,6.5,0.));
#9577=CARTESIAN_POINT('Origin',(4.,6.,0.));
#9578=CARTESIAN_POINT('Origin',(4.,6.,-0.5));
#11827=UNCERTAINTY_MEASURE_WITH_UNIT(LENGTH_MEASURE(0.001),#11917,
'DISTANCE_ACCURACY_VALUE',
'Maximum model space distance between geometric entities at asserted c
onnectivities');
#11869=UNCERTAINTY_MEASURE_WITH_UNIT(LENGTH_MEASURE(0.001),#11917,
'DISTANCE_ACCURACY_VALUE',
'Maximum model space distance between geometric entities at asserted c
onnectivities');
#11874=(
GEOMETRIC_REPRESENTATION_CONTEXT(3)
GLOBAL_UNCERTAINTY_ASSIGNED_CONTEXT((#11827))
GLOBAL_UNIT_ASSIGNED_CONTEXT((#11917,#11919,#11920))
REPRESENTATION_CONTEXT('','3D')
);
#11916=(
GEOMETRIC_REPRESENTATION_CONTEXT(3)
GLOBAL_UNCERTAINTY_ASSIGNED_CONTEXT((#11869))
GLOBAL_UNIT_ASSIGNED_CONTEXT((#11917,#11919,#11920))
REPRESENTATION_CONTEXT('','3D')
);
#11917=(
LENGTH_UNIT()
NAMED_UNIT(*)
SI_UNIT(.CENTI.,.METRE.)
);
#11919=(
NAMED_UNIT(*)
PLANE_ANGLE_UNIT()
SI_UNIT($,.RADIAN.)
);
#11920=(
NAMED_UNIT(*)
SI_UNIT($,.STERADIAN.)
SOLID_ANGLE_UNIT()
);
#11925=SHAPE_DEFINITION_REPRESENTATION(#11971,#12083);
#11971=PRODUCT_DEFINITION_SHAPE('',$,#12130);
#12083=SHAPE_REPRESENTATION('',(#6599),#11874);
#12125=PRODUCT_DEFINITION_CONTEXT('part definition',#12265,'design');
#12130=PRODUCT_DEFINITION('Foot strip (1)','Foot strip (1)',#12176,#12125);
#12176=PRODUCT_DEFINITION_FORMATION('',$,#12271);
#12265=APPLICATION_CONTEXT(
'Core Data for Automotive Mechanical Design Process');
#12266=PRODUCT_CONTEXT('part definition',#12265,'mechanical');
#12271=PRODUCT('Foot strip (1)','Foot strip (1)','Foot strip (1)',(#12266));
#12355=COLOUR_RGB('Light Blue',0.38,0.62,0.78);
#12356=FILL_AREA_STYLE_COLOUR('',#12355);
#12357=FILL_AREA_STYLE('',(#12356));
#12358=SURFACE_STYLE_FILL_AREA(#12357);
#12359=SURFACE_SIDE_STYLE('',(#12358));
#12360=SURFACE_STYLE_USAGE(.BOTH.,#12359);
#12361=PRESENTATION_STYLE_ASSIGNMENT((#12360));
ENDSEC;
END-ISO-10303-21;
